ISO-10303-21;
HEADER;
/* Generated by software containing ST-Developer
 * from STEP Tools, Inc. (www.steptools.com) 
 */

FILE_DESCRIPTION(
/* description */ ('Gravity roller conveyor section'),
/* implementation_level */ '2;1');

FILE_NAME(
/* name */ 'Inner race spacer (1).step',
/* time_stamp */ '2026-11-02T07:43:02-08:00',
/* author */ (''),
/* organization */ (''),
/* preprocessor_version */ 'ST-DEVELOPER v20.2',
/* originating_system */ 'Autodesk Translation Framework v15.17.0.0',
/* authorisation */ '');

FILE_SCHEMA (('AUTOMOTIVE_DESIGN { 1 0 10303 214 3 1 1 }'));
ENDSEC;

DATA;
#10=MECHANICAL_DESIGN_GEOMETRIC_PRESENTATION_REPRESENTATION('',(#565),#13821);
#489=SHAPE_REPRESENTATION_RELATIONSHIP('SRR','None',#14028,#523);
#523=ADVANCED_BREP_SHAPE_REPRESENTATION('',(#605),#13815);
#565=STYLED_ITEM('',(#14191),#605);
#605=MANIFOLD_SOLID_BREP('Body1',#7665);
#687=FACE_BOUND('',#1859,.T.);
#688=FACE_BOUND('',#1861,.T.);
#960=PLANE('',#8624);
#961=PLANE('',#8625);
#1359=FACE_OUTER_BOUND('',#1856,.T.);
#1360=FACE_OUTER_BOUND('',#1857,.T.);
#1361=FACE_OUTER_BOUND('',#1858,.T.);
#1362=FACE_OUTER_BOUND('',#1860,.T.);
#1856=EDGE_LOOP('',(#6854,#6855,#6856,#6857));
#1857=EDGE_LOOP('',(#6858,#6859,#6860,#6861));
#1858=EDGE_LOOP('',(#6862));
#1859=EDGE_LOOP('',(#6863));
#1860=EDGE_LOOP('',(#6864));
#1861=EDGE_LOOP('',(#6865));
#2556=LINE('',#13359,#3274);
#2557=LINE('',#13365,#3275);
#3274=VECTOR('',#10579,0.505);
#3275=VECTOR('',#10586,0.7);
#3554=CIRCLE('',#8619,0.505);
#3555=CIRCLE('',#8620,0.505);
#3556=CIRCLE('',#8622,0.7);
#3557=CIRCLE('',#8623,0.7);
#4148=VERTEX_POINT('',#13356);
#4149=VERTEX_POINT('',#13358);
#4150=VERTEX_POINT('',#13362);
#4151=VERTEX_POINT('',#13364);
#5064=EDGE_CURVE('',#4148,#4148,#3554,.T.);
#5065=EDGE_CURVE('',#4148,#4149,#2556,.T.);
#5066=EDGE_CURVE('',#4149,#4149,#3555,.T.);
#5067=EDGE_CURVE('',#4150,#4150,#3556,.T.);
#5068=EDGE_CURVE('',#4150,#4151,#2557,.T.);
#5069=EDGE_CURVE('',#4151,#4151,#3557,.T.);
#6854=ORIENTED_EDGE('',*,*,#5064,.F.);
#6855=ORIENTED_EDGE('',*,*,#5065,.T.);
#6856=ORIENTED_EDGE('',*,*,#5066,.T.);
#6857=ORIENTED_EDGE('',*,*,#5065,.F.);
#6858=ORIENTED_EDGE('',*,*,#5067,.F.);
#6859=ORIENTED_EDGE('',*,*,#5068,.T.);
#6860=ORIENTED_EDGE('',*,*,#5069,.T.);
#6861=ORIENTED_EDGE('',*,*,#5068,.F.);
#6862=ORIENTED_EDGE('',*,*,#5067,.T.);
#6863=ORIENTED_EDGE('',*,*,#5064,.T.);
#6864=ORIENTED_EDGE('',*,*,#5069,.F.);
#6865=ORIENTED_EDGE('',*,*,#5066,.F.);
#7194=CYLINDRICAL_SURFACE('',#8618,0.505);
#7195=CYLINDRICAL_SURFACE('',#8621,0.7);
#7560=ADVANCED_FACE('',(#1359),#7194,.F.);
#7561=ADVANCED_FACE('',(#1360),#7195,.T.);
#7562=ADVANCED_FACE('',(#1361,#687),#960,.T.);
#7563=ADVANCED_FACE('',(#1362,#688),#961,.F.);
#7665=CLOSED_SHELL('',(#7560,#7561,#7562,#7563));
#8617=AXIS2_PLACEMENT_3D('',#13354,#10573,#10574);
#8618=AXIS2_PLACEMENT_3D('',#13355,#10575,#10576);
#8619=AXIS2_PLACEMENT_3D('',#13357,#10577,#10578);
#8620=AXIS2_PLACEMENT_3D('',#13360,#10580,#10581);
#8621=AXIS2_PLACEMENT_3D('',#13361,#10582,#10583);
#8622=AXIS2_PLACEMENT_3D('',#13363,#10584,#10585);
#8623=AXIS2_PLACEMENT_3D('',#13366,#10587,#10588);
#8624=AXIS2_PLACEMENT_3D('',#13367,#10589,#10590);
#8625=AXIS2_PLACEMENT_3D('',#13368,#10591,#10592);
#10573=DIRECTION('axis',(0.,0.,1.));
#10574=DIRECTION('refdir',(1.,0.,0.));
#10575=DIRECTION('center_axis',(0.,1.,0.));
#10576=DIRECTION('ref_axis',(1.,0.,0.));
#10577=DIRECTION('center_axis',(0.,-1.,0.));
#10578=DIRECTION('ref_axis',(1.,0.,0.));
#10579=DIRECTION('',(0.,-1.,0.));
#10580=DIRECTION('center_axis',(0.,-1.,0.));
#10581=DIRECTION('ref_axis',(1.,0.,0.));
#10582=DIRECTION('center_axis',(0.,1.,0.));
#10583=DIRECTION('ref_axis',(1.,0.,0.));
#10584=DIRECTION('center_axis',(0.,1.,0.));
#10585=DIRECTION('ref_axis',(1.,0.,0.));
#10586=DIRECTION('',(0.,-1.,0.));
#10587=DIRECTION('center_axis',(0.,1.,0.));
#10588=DIRECTION('ref_axis',(1.,0.,0.));
#10589=DIRECTION('center_axis',(0.,1.,0.));
#10590=DIRECTION('ref_axis',(1.,0.,0.));
#10591=DIRECTION('center_axis',(0.,1.,0.));
#10592=DIRECTION('ref_axis',(1.,0.,0.));
#13354=CARTESIAN_POINT('',(0.,0.,0.));
#13355=CARTESIAN_POINT('Origin',(3.,29.95,8.));
#13356=CARTESIAN_POINT('',(2.495,31.,8.));
#13357=CARTESIAN_POINT('Origin',(3.,31.,8.));
#13358=CARTESIAN_POINT('',(2.495,29.95,8.));
#13359=CARTESIAN_POINT('',(2.495,29.95,8.));
#13360=CARTESIAN_POINT('Origin',(3.,29.95,8.));
#13361=CARTESIAN_POINT('Origin',(3.,29.95,8.));
#13362=CARTESIAN_POINT('',(2.3,31.,8.));
#13363=CARTESIAN_POINT('Origin',(3.,31.,8.));
#13364=CARTESIAN_POINT('',(2.3,29.95,8.));
#13365=CARTESIAN_POINT('',(2.3,29.95,8.));
#13366=CARTESIAN_POINT('Origin',(3.,29.95,8.));
#13367=CARTESIAN_POINT('Origin',(3.,31.,8.));
#13368=CARTESIAN_POINT('Origin',(3.,29.95,8.));
#13776=UNCERTAINTY_MEASURE_WITH_UNIT(LENGTH_MEASURE(0.001),#13822,
'DISTANCE_ACCURACY_VALUE',
'Maximum model space distance between geometric entities at asserted c
onnectivities');
#13782=UNCERTAINTY_MEASURE_WITH_UNIT(LENGTH_MEASURE(0.001),#13822,
'DISTANCE_ACCURACY_VALUE',
'Maximum model space distance between geometric entities at asserted c
onnectivities');
#13815=(
GEOMETRIC_REPRESENTATION_CONTEXT(3)
GLOBAL_UNCERTAINTY_ASSIGNED_CONTEXT((#13776))
GLOBAL_UNIT_ASSIGNED_CONTEXT((#13822,#13824,#13825))
REPRESENTATION_CONTEXT('','3D')
);
#13821=(
GEOMETRIC_REPRESENTATION_CONTEXT(3)
GLOBAL_UNCERTAINTY_ASSIGNED_CONTEXT((#13782))
GLOBAL_UNIT_ASSIGNED_CONTEXT((#13822,#13824,#13825))
REPRESENTATION_CONTEXT('','3D')
);
#13822=(
LENGTH_UNIT()
NAMED_UNIT(*)
SI_UNIT(.CENTI.,.METRE.)
);
#13824=(
NAMED_UNIT(*)
PLANE_ANGLE_UNIT()
SI_UNIT($,.RADIAN.)
);
#13825=(
NAMED_UNIT(*)
SI_UNIT($,.STERADIAN.)
SOLID_ANGLE_UNIT()
);
#13858=SHAPE_DEFINITION_REPRESENTATION(#13901,#14028);
#13901=PRODUCT_DEFINITION_SHAPE('',$,#14067);
#14028=SHAPE_REPRESENTATION('',(#8617),#13815);
#14034=PRODUCT_DEFINITION_CONTEXT('part definition',#14150,'design');
#14067=PRODUCT_DEFINITION('Inner race spacer_1','Inner race spacer (1)',
#14105,#14034);
#14105=PRODUCT_DEFINITION_FORMATION('',$,#14184);
#14150=APPLICATION_CONTEXT(
'Core Data for Automotive Mechanical Design Process');
#14151=PRODUCT_CONTEXT('part definition',#14150,'mechanical');
#14184=PRODUCT('Inner race spacer_1','Inner race spacer (1)',
'Inner race spacer',(#14151));
#14191=PRESENTATION_STYLE_ASSIGNMENT((#14196));
#14196=SURFACE_STYLE_USAGE(.BOTH.,#14201);
#14201=SURFACE_SIDE_STYLE('',(#14206));
#14206=SURFACE_STYLE_FILL_AREA(#14211);
#14211=FILL_AREA_STYLE('CAD Library Painted - Steel gray',(#14216));
#14216=FILL_AREA_STYLE_COLOUR('CAD Library Painted - Steel gray',#14221);
#14221=COLOUR_RGB('CAD Library Painted - Steel gray',0.592156862745098,
0.631372549019608,0.67843137254902);
ENDSEC;
END-ISO-10303-21;
